ISO-10303-21;
HEADER;
FILE_DESCRIPTION (('STEP AP214'),
    '1' );
FILE_NAME ('key.step',
    '2026-10-26T19:46:16',
    ( '' ),
    ( '' ),
    'SwSTEP 2.0',
    'SolidWorks 2025',
    '' );
FILE_SCHEMA (( 'AUTOMOTIVE_DESIGN' ));
ENDSEC;

DATA;
#633=CARTESIAN_POINT ( 'NONE',  ( -2.250000000000000888, -2.250000000000000000, 28.00000000000000000 ) ) ;
#1902=EDGE_CURVE ( 'NONE', #53551, #15239, #48559, .T. ) ;
#2404=ORIENTED_EDGE ( 'NONE', *, *, #58904, .F. ) ;
#2847=APPLICATION_CONTEXT ( 'automotive_design' ) ;
#2927=DIRECTION ( 'NONE',  ( -0.000000000000000000, -0.000000000000000000, -1.000000000000000000 ) ) ;
#3153=ORIENTED_EDGE ( 'NONE', *, *, #45763, .T. ) ;
#4157=PRODUCT ( 'key', 'key', '', ( #45946 ) ) ;
#4319=ADVANCED_FACE ( 'NONE', ( #26724 ), #38808, .F. ) ;
#4494=ORIENTED_EDGE ( 'NONE', *, *, #11398, .T. ) ;
#4599=ORIENTED_EDGE ( 'NONE', *, *, #11136, .T. ) ;
#4980=DIRECTION ( 'NONE',  ( 1.000000000000000000, 9.637352644315595243E-17, 0.000000000000000000 ) ) ;
#5958=DIRECTION ( 'NONE',  ( -1.000000000000000000, -9.637352644315595243E-17, 0.000000000000000000 ) ) ;
#6084=VECTOR ( 'NONE', #30382, 1000.000000000000000 ) ;
#6275=EDGE_CURVE ( 'NONE', #50334, #66510, #58329, .T. ) ;
#6285=PRODUCT_DEFINITION ( 'UNKNOWN', '', #67084, #22915 ) ;
#6635=CARTESIAN_POINT ( 'NONE',  ( 2.249999999999999112, -2.249999999999999556, 0.000000000000000000 ) ) ;
#6702=FACE_OUTER_BOUND ( 'NONE', #58851, .T. ) ;
#7416=VECTOR ( 'NONE', #64833, 1000.000000000000000 ) ;
#8785=PLANE ( 'NONE',  #13972 ) ;
#8812=ORIENTED_EDGE ( 'NONE', *, *, #6275, .T. ) ;
#8882=CARTESIAN_POINT ( 'NONE',  ( 2.249999999999999112, -2.249999999999999556, 0.000000000000000000 ) ) ;
#8906=VECTOR ( 'NONE', #34645, 1000.000000000000000 ) ;
#8987=EDGE_LOOP ( 'NONE', ( #8812, #59289, #54791, #30260 ) ) ;
#9622=CARTESIAN_POINT ( 'NONE',  ( 0.000000000000000000, 0.000000000000000000, 28.00000000000000000 ) ) ;
#10631=LINE ( 'NONE', #56664, #47956 ) ;
#10726=DIRECTION ( 'NONE',  ( 0.000000000000000000, 0.000000000000000000, 1.000000000000000000 ) ) ;
#10783=PRODUCT_DEFINITION_SHAPE ( 'NONE', 'NONE',  #6285 ) ;
#10842=ORIENTED_EDGE ( 'NONE', *, *, #39892, .T. ) ;
#11136=EDGE_CURVE ( 'NONE', #52491, #50334, #16127, .T. ) ;
#11398=EDGE_CURVE ( 'NONE', #17643, #53551, #53090, .T. ) ;
#11422=DIRECTION ( 'NONE',  ( 0.000000000000000000, 0.000000000000000000, 1.000000000000000000 ) ) ;
#12148=VECTOR ( 'NONE', #35114, 1000.000000000000000 ) ;
#12887=SHAPE_REPRESENTATION_RELATIONSHIP ( 'NONE' , 'NONE' ,  #63845, #58002 ) ;
#13052=EDGE_CURVE ( 'NONE', #37692, #50334, #41599, .T. ) ;
#13972=AXIS2_PLACEMENT_3D ( 'NONE', #26875, #27241, #49890 ) ;
#14070=EDGE_CURVE ( 'NONE', #66510, #15239, #23974, .T. ) ;
#14566=AXIS2_PLACEMENT_3D ( 'NONE', #9622, #10726, #56023 ) ;
#15128=LINE ( 'NONE', #40751, #12148 ) ;
#15239=VERTEX_POINT ( 'NONE', #62957 ) ;
#15329=VECTOR ( 'NONE', #70358, 1000.000000000000000 ) ;
#15680=LINE ( 'NONE', #49268, #42560 ) ;
#16127=LINE ( 'NONE', #62914, #73952 ) ;
#16141=CARTESIAN_POINT ( 'NONE',  ( -2.250000000000000888, 2.250000000000000000, 28.00000000000000000 ) ) ;
#16909=AXIS2_PLACEMENT_3D ( 'NONE', #33164, #45201, #73494 ) ;
#17292=LINE ( 'NONE', #57681, #56496 ) ;
#17487=ADVANCED_FACE ( 'NONE', ( #67705 ), #62399, .T. ) ;
#17643=VERTEX_POINT ( 'NONE', #29313 ) ;
#18015=CARTESIAN_POINT ( 'NONE',  ( -2.250000000000000888, 2.250000000000000000, 28.00000000000000000 ) ) ;
#20124=ORIENTED_EDGE ( 'NONE', *, *, #14070, .F. ) ;
#21039=CARTESIAN_POINT ( 'NONE',  ( 2.249999999999999112, -2.249999999999999556, 28.00000000000000000 ) ) ;
#21424=AXIS2_PLACEMENT_3D ( 'NONE', #633, #27783, #63601 ) ;
#22169=DIRECTION ( 'NONE',  ( 1.000000000000000000, 9.637352644315595243E-17, 0.000000000000000000 ) ) ;
#22915=PRODUCT_DEFINITION_CONTEXT ( 'detailed design', #50101, 'design' ) ;
#22951=ORIENTED_EDGE ( 'NONE', *, *, #1902, .F. ) ;
#23469=AXIS2_PLACEMENT_3D ( 'NONE', #46679, #58397, #5958 ) ;
#23974=LINE ( 'NONE', #70736, #6084 ) ;
#24320=LINE ( 'NONE', #53378, #15329 ) ;
#26724=FACE_OUTER_BOUND ( 'NONE', #8987, .T. ) ;
#26818=VECTOR ( 'NONE', #2927, 1000.000000000000000 ) ;
#26875=CARTESIAN_POINT ( 'NONE',  ( -2.250000000000000888, 2.250000000000000000, 28.00000000000000000 ) ) ;
#27241=DIRECTION ( 'NONE',  ( 0.000000000000000000, -1.000000000000000000, 0.000000000000000000 ) ) ;
#27417=ORIENTED_EDGE ( 'NONE', *, *, #13052, .F. ) ;
#27783=DIRECTION ( 'NONE',  ( 1.000000000000000000, 0.000000000000000000, 0.000000000000000000 ) ) ;
#27827=EDGE_LOOP ( 'NONE', ( #42686, #2404, #65276, #39882 ) ) ;
#28991=DIRECTION ( 'NONE',  ( -0.000000000000000000, -1.000000000000000000, -0.000000000000000000 ) ) ;
#29173=CARTESIAN_POINT ( 'NONE',  ( 2.249999999999999112, -2.249999999999999556, 28.00000000000000000 ) ) ;
#29287=PLANE ( 'NONE',  #21424 ) ;
#29313=CARTESIAN_POINT ( 'NONE',  ( 2.249999999999999112, 2.250000000000000000, 28.00000000000000000 ) ) ;
#29640=DIRECTION ( 'NONE',  ( 0.000000000000000000, 1.000000000000000000, 0.000000000000000000 ) ) ;
#30260=ORIENTED_EDGE ( 'NONE', *, *, #13052, .T. ) ;
#30382=DIRECTION ( 'NONE',  ( -1.000000000000000000, -0.000000000000000000, -0.000000000000000000 ) ) ;
#30566=( NAMED_UNIT ( * ) SI_UNIT ( $, .STERADIAN. ) SOLID_ANGLE_UNIT ( ) );
#30874=CARTESIAN_POINT ( 'NONE',  ( 2.249999999999999112, -2.249999999999999556, 28.00000000000000000 ) ) ;
#32098=ORIENTED_EDGE ( 'NONE', *, *, #33351, .F. ) ;
#32210=ORIENTED_EDGE ( 'NONE', *, *, #58904, .T. ) ;
#33164=CARTESIAN_POINT ( 'NONE',  ( 2.249999999999999112, -2.249999999999999556, 28.00000000000000000 ) ) ;
#33351=EDGE_CURVE ( 'NONE', #60808, #37692, #10631, .T. ) ;
#34459=DIRECTION ( 'NONE',  ( 1.000000000000000000, 0.000000000000000000, 0.000000000000000000 ) ) ;
#34483=ADVANCED_FACE ( 'NONE', ( #64142 ), #53565, .F. ) ;
#34645=DIRECTION ( 'NONE',  ( -1.000000000000000000, -0.000000000000000000, -0.000000000000000000 ) ) ;
#35114=DIRECTION ( 'NONE',  ( -0.000000000000000000, -0.000000000000000000, -1.000000000000000000 ) ) ;
#35507=CARTESIAN_POINT ( 'NONE',  ( -2.250000000000000888, -2.250000000000000000, 28.00000000000000000 ) ) ;
#35922=( NAMED_UNIT ( * ) PLANE_ANGLE_UNIT ( ) SI_UNIT ( $, .RADIAN. ) );
#35923=MECHANICAL_DESIGN_GEOMETRIC_PRESENTATION_REPRESENTATION('',(#64842),#67208);
#36740=ADVANCED_FACE ( 'NONE', ( #61586 ), #8785, .F. ) ;
#37692=VERTEX_POINT ( 'NONE', #21039 ) ;
#37943=VECTOR ( 'NONE', #64614, 1000.000000000000000 ) ;
#38230=CLOSED_SHELL ( 'NONE', ( #36740, #41700, #66186, #4319, #17487, #34483 ) ) ;
#38722=DIRECTION ( 'NONE',  ( -0.000000000000000000, -1.000000000000000000, -0.000000000000000000 ) ) ;
#38808=PLANE ( 'NONE',  #16909 ) ;
#39114=( LENGTH_UNIT ( ) NAMED_UNIT ( * ) SI_UNIT ( .MILLI., .METRE. ) );
#39882=ORIENTED_EDGE ( 'NONE', *, *, #1902, .T. ) ;
#39892=EDGE_CURVE ( 'NONE', #17643, #66510, #24320, .T. ) ;
#40058=ORIENTED_EDGE ( 'NONE', *, *, #33351, .T. ) ;
#40549=UNCERTAINTY_MEASURE_WITH_UNIT (LENGTH_MEASURE( 1.000000000000000082E-05 ), #52528, 'distance_accuracy_value', 'NONE');
#40751=CARTESIAN_POINT ( 'NONE',  ( -2.250000000000000888, -2.250000000000000000, 28.00000000000000000 ) ) ;
#40799=EDGE_LOOP ( 'NONE', ( #61599, #22951, #57797, #10842 ) ) ;
#41104=ORIENTED_EDGE ( 'NONE', *, *, #60489, .T. ) ;
#41120=ORIENTED_EDGE ( 'NONE', *, *, #11136, .F. ) ;
#41383=MANIFOLD_SOLID_BREP ( 'Boss-Extrude1', #38230 ) ;
#41599=LINE ( 'NONE', #29173, #37943 ) ;
#41700=ADVANCED_FACE ( 'NONE', ( #74179 ), #29287, .F. ) ;
#42558=LINE ( 'NONE', #30874, #7416 ) ;
#42560=VECTOR ( 'NONE', #38722, 1000.000000000000000 ) ;
#42686=ORIENTED_EDGE ( 'NONE', *, *, #53198, .T. ) ;
#45201=DIRECTION ( 'NONE',  ( -1.000000000000000000, 0.000000000000000000, 0.000000000000000000 ) ) ;
#45763=EDGE_CURVE ( 'NONE', #37692, #17643, #42558, .T. ) ;
#45946=PRODUCT_CONTEXT ( 'NONE', #2847, 'mechanical' ) ;
#46679=CARTESIAN_POINT ( 'NONE',  ( -2.250000000000000888, -2.250000000000000000, 28.00000000000000000 ) ) ;
#47149=DIRECTION ( 'NONE',  ( 1.000000000000000000, 0.000000000000000000, -0.000000000000000000 ) ) ;
#47956=VECTOR ( 'NONE', #4980, 1000.000000000000000 ) ;
#48559=LINE ( 'NONE', #66667, #26818 ) ;
#49268=CARTESIAN_POINT ( 'NONE',  ( -2.250000000000000888, -2.250000000000000000, 0.000000000000000000 ) ) ;
#49890=DIRECTION ( 'NONE',  ( 0.000000000000000000, -0.000000000000000000, -1.000000000000000000 ) ) ;
#50101=APPLICATION_CONTEXT ( 'automotive_design' ) ;
#50334=VERTEX_POINT ( 'NONE', #8882 ) ;
#51304=( GEOMETRIC_REPRESENTATION_CONTEXT ( 3 ) GLOBAL_UNCERTAINTY_ASSIGNED_CONTEXT ( ( #40549 ) ) GLOBAL_UNIT_ASSIGNED_CONTEXT ( ( #52528, #35922, #64944 ) ) REPRESENTATION_CONTEXT ( 'NONE', 'WORKASPACE' ) );
#52491=VERTEX_POINT ( 'NONE', #55213 ) ;
#52528=( LENGTH_UNIT ( ) NAMED_UNIT ( * ) SI_UNIT ( .MILLI., .METRE. ) );
#53090=LINE ( 'NONE', #18015, #8906 ) ;
#53198=EDGE_CURVE ( 'NONE', #15239, #52491, #15680, .T. ) ;
#53378=CARTESIAN_POINT ( 'NONE',  ( 2.249999999999999112, 2.250000000000000000, 28.00000000000000000 ) ) ;
#53551=VERTEX_POINT ( 'NONE', #16141 ) ;
#53565=PLANE ( 'NONE',  #62447 ) ;
#54791=ORIENTED_EDGE ( 'NONE', *, *, #45763, .F. ) ;
#55213=CARTESIAN_POINT ( 'NONE',  ( -2.250000000000000888, -2.250000000000000000, 0.000000000000000000 ) ) ;
#56023=DIRECTION ( 'NONE',  ( 1.000000000000000000, 0.000000000000000000, -0.000000000000000000 ) ) ;
#56496=VECTOR ( 'NONE', #28991, 1000.000000000000000 ) ;
#56534=SHAPE_DEFINITION_REPRESENTATION ( #10783, #63845 ) ;
#56664=CARTESIAN_POINT ( 'NONE',  ( -2.250000000000000888, -2.250000000000000000, 28.00000000000000000 ) ) ;
#57354=AXIS2_PLACEMENT_3D ( 'NONE', #63097, #11422, #34459 ) ;
#57652=PLANE ( 'NONE',  #23469 ) ;
#57681=CARTESIAN_POINT ( 'NONE',  ( -2.250000000000000888, -2.250000000000000000, 28.00000000000000000 ) ) ;
#57797=ORIENTED_EDGE ( 'NONE', *, *, #11398, .F. ) ;
#58002=ADVANCED_BREP_SHAPE_REPRESENTATION ( '', ( #41383, #57354 ), #51304 ) ;
#58329=LINE ( 'NONE', #6635, #65205 ) ;
#58397=DIRECTION ( 'NONE',  ( -9.637352644315595243E-17, 1.000000000000000000, 0.000000000000000000 ) ) ;
#58496=CARTESIAN_POINT ( 'NONE',  ( 0.000000000000000000, 0.000000000000000000, 0.000000000000000000 ) ) ;
#58851=EDGE_LOOP ( 'NONE', ( #4599, #27417, #32098, #32210 ) ) ;
#58904=EDGE_CURVE ( 'NONE', #60808, #52491, #15128, .T. ) ;
#59289=ORIENTED_EDGE ( 'NONE', *, *, #39892, .F. ) ;
#60489=EDGE_CURVE ( 'NONE', #53551, #60808, #17292, .T. ) ;
#60808=VERTEX_POINT ( 'NONE', #35507 ) ;
#61292=EDGE_LOOP ( 'NONE', ( #4494, #41104, #40058, #3153 ) ) ;
#61586=FACE_OUTER_BOUND ( 'NONE', #40799, .T. ) ;
#61599=ORIENTED_EDGE ( 'NONE', *, *, #14070, .T. ) ;
#62399=PLANE ( 'NONE',  #14566 ) ;
#62447=AXIS2_PLACEMENT_3D ( 'NONE', #58496, #64876, #47149 ) ;
#62914=CARTESIAN_POINT ( 'NONE',  ( -2.250000000000000888, -2.250000000000000000, 0.000000000000000000 ) ) ;
#62957=CARTESIAN_POINT ( 'NONE',  ( -2.250000000000000888, 2.250000000000000000, 0.000000000000000000 ) ) ;
#63097=CARTESIAN_POINT ( 'NONE',  ( 0.000000000000000000, 0.000000000000000000, 0.000000000000000000 ) ) ;
#63601=DIRECTION ( 'NONE',  ( 0.000000000000000000, 0.000000000000000000, -1.000000000000000000 ) ) ;
#63845=SHAPE_REPRESENTATION ( 'key', ( #57354 ), #51304 ) ;
#64142=FACE_OUTER_BOUND ( 'NONE', #73723, .T. ) ;
#64614=DIRECTION ( 'NONE',  ( -0.000000000000000000, -0.000000000000000000, -1.000000000000000000 ) ) ;
#64833=DIRECTION ( 'NONE',  ( 0.000000000000000000, 1.000000000000000000, 0.000000000000000000 ) ) ;
#64842=STYLED_ITEM('',(#74699),#41383);
#64876=DIRECTION ( 'NONE',  ( 0.000000000000000000, 0.000000000000000000, 1.000000000000000000 ) ) ;
#64944=( NAMED_UNIT ( * ) SI_UNIT ( $, .STERADIAN. ) SOLID_ANGLE_UNIT ( ) );
#65205=VECTOR ( 'NONE', #29640, 1000.000000000000000 ) ;
#65276=ORIENTED_EDGE ( 'NONE', *, *, #60489, .F. ) ;
#65631=( NAMED_UNIT ( * ) PLANE_ANGLE_UNIT ( ) SI_UNIT ( $, .RADIAN. ) );
#65889=CARTESIAN_POINT ( 'NONE',  ( 2.249999999999999112, 2.250000000000000000, 0.000000000000000000 ) ) ;
#66186=ADVANCED_FACE ( 'NONE', ( #6702 ), #57652, .F. ) ;
#66510=VERTEX_POINT ( 'NONE', #65889 ) ;
#66667=CARTESIAN_POINT ( 'NONE',  ( -2.250000000000000888, 2.250000000000000000, 28.00000000000000000 ) ) ;
#67084=PRODUCT_DEFINITION_FORMATION_WITH_SPECIFIED_SOURCE ( 'ANY', '', #4157, .NOT_KNOWN. ) ;
#67208=( GEOMETRIC_REPRESENTATION_CONTEXT ( 3 ) GLOBAL_UNCERTAINTY_ASSIGNED_CONTEXT ( ( #69488 ) ) GLOBAL_UNIT_ASSIGNED_CONTEXT ( ( #39114, #65631, #30566 ) ) REPRESENTATION_CONTEXT ( 'NONE', 'WORKASPACE' ) );
#67705=FACE_OUTER_BOUND ( 'NONE', #61292, .T. ) ;
#68336=ORIENTED_EDGE ( 'NONE', *, *, #6275, .F. ) ;
#69141=ORIENTED_EDGE ( 'NONE', *, *, #53198, .F. ) ;
#69488=UNCERTAINTY_MEASURE_WITH_UNIT (LENGTH_MEASURE( 1.000000000000000082E-05 ), #39114, 'distance_accuracy_value', 'NONE');
#70358=DIRECTION ( 'NONE',  ( -0.000000000000000000, -0.000000000000000000, -1.000000000000000000 ) ) ;
#70736=CARTESIAN_POINT ( 'NONE',  ( -2.250000000000000888, 2.250000000000000000, 0.000000000000000000 ) ) ;
#73494=DIRECTION ( 'NONE',  ( 0.000000000000000000, 0.000000000000000000, 1.000000000000000000 ) ) ;
#73723=EDGE_LOOP ( 'NONE', ( #20124, #68336, #41120, #69141 ) ) ;
#73952=VECTOR ( 'NONE', #22169, 1000.000000000000000 ) ;
#74179=FACE_OUTER_BOUND ( 'NONE', #27827, .T. ) ;
#74693=COLOUR_RGB('Grey',0.48,0.52,0.57);
#74694=FILL_AREA_STYLE_COLOUR('',#74693);
#74695=FILL_AREA_STYLE('',(#74694));
#74696=SURFACE_STYLE_FILL_AREA(#74695);
#74697=SURFACE_SIDE_STYLE('',(#74696));
#74698=SURFACE_STYLE_USAGE(.BOTH.,#74697);
#74699=PRESENTATION_STYLE_ASSIGNMENT((#74698));
ENDSEC;
END-ISO-10303-21;
